ISO-10303-21;
HEADER;
/* Generated by software containing ST-Developer
 * from STEP Tools, Inc. (www.steptools.com) 
 */

FILE_DESCRIPTION(
/* description */ ('Gravity roller conveyor section'),
/* implementation_level */ '2;1');

FILE_NAME(
/* name */ 'Bearing retainer (1).step',
/* time_stamp */ '2026-11-02T07:43:02-08:00',
/* author */ (''),
/* organization */ (''),
/* preprocessor_version */ 'ST-DEVELOPER v20.2',
/* originating_system */ 'Autodesk Translation Framework v15.17.0.0',
/* authorisation */ '');

FILE_SCHEMA (('AUTOMOTIVE_DESIGN { 1 0 10303 214 3 1 1 }'));
ENDSEC;

DATA;
#10=MECHANICAL_DESIGN_GEOMETRIC_PRESENTATION_REPRESENTATION('',(#547),#13821);
#479=SHAPE_REPRESENTATION_RELATIONSHIP('SRR','None',#14017,#513);
#513=ADVANCED_BREP_SHAPE_REPRESENTATION('',(#587),#13804);
#547=STYLED_ITEM('',(#14191),#587);
#587=MANIFOLD_SOLID_BREP('Body1',#7647);
#661=FACE_BOUND('',#1747,.T.);
#662=FACE_BOUND('',#1751,.T.);
#663=FACE_BOUND('',#1753,.T.);
#924=PLANE('',#8418);
#925=PLANE('',#8425);
#926=PLANE('',#8426);
#1274=FACE_OUTER_BOUND('',#1745,.T.);
#1275=FACE_OUTER_BOUND('',#1746,.T.);
#1276=FACE_OUTER_BOUND('',#1748,.T.);
#1277=FACE_OUTER_BOUND('',#1749,.T.);
#1278=FACE_OUTER_BOUND('',#1750,.T.);
#1279=FACE_OUTER_BOUND('',#1752,.T.);
#1745=EDGE_LOOP('',(#6528,#6529,#6530,#6531));
#1746=EDGE_LOOP('',(#6532));
#1747=EDGE_LOOP('',(#6533));
#1748=EDGE_LOOP('',(#6534,#6535,#6536,#6537));
#1749=EDGE_LOOP('',(#6538,#6539,#6540,#6541));
#1750=EDGE_LOOP('',(#6542));
#1751=EDGE_LOOP('',(#6543));
#1752=EDGE_LOOP('',(#6544));
#1753=EDGE_LOOP('',(#6545));
#2513=LINE('',#12639,#3231);
#2514=LINE('',#12647,#3232);
#2515=LINE('',#12652,#3233);
#3231=VECTOR('',#10130,1.5);
#3232=VECTOR('',#10141,1.2);
#3233=VECTOR('',#10146,2.);
#3452=CIRCLE('',#8416,1.5);
#3453=CIRCLE('',#8417,1.5);
#3454=CIRCLE('',#8419,1.2);
#3455=CIRCLE('',#8421,1.2);
#3456=CIRCLE('',#8423,2.);
#3457=CIRCLE('',#8424,2.);
#4030=VERTEX_POINT('',#12636);
#4031=VERTEX_POINT('',#12638);
#4032=VERTEX_POINT('',#12642);
#4033=VERTEX_POINT('',#12645);
#4034=VERTEX_POINT('',#12649);
#4035=VERTEX_POINT('',#12651);
#4901=EDGE_CURVE('',#4030,#4030,#3452,.T.);
#4902=EDGE_CURVE('',#4030,#4031,#2513,.T.);
#4903=EDGE_CURVE('',#4031,#4031,#3453,.T.);
#4904=EDGE_CURVE('',#4032,#4032,#3454,.T.);
#4905=EDGE_CURVE('',#4033,#4033,#3455,.T.);
#4906=EDGE_CURVE('',#4033,#4032,#2514,.T.);
#4907=EDGE_CURVE('',#4034,#4034,#3456,.T.);
#4908=EDGE_CURVE('',#4034,#4035,#2515,.T.);
#4909=EDGE_CURVE('',#4035,#4035,#3457,.T.);
#6528=ORIENTED_EDGE('',*,*,#4901,.F.);
#6529=ORIENTED_EDGE('',*,*,#4902,.T.);
#6530=ORIENTED_EDGE('',*,*,#4903,.T.);
#6531=ORIENTED_EDGE('',*,*,#4902,.F.);
#6532=ORIENTED_EDGE('',*,*,#4901,.T.);
#6533=ORIENTED_EDGE('',*,*,#4904,.F.);
#6534=ORIENTED_EDGE('',*,*,#4905,.F.);
#6535=ORIENTED_EDGE('',*,*,#4906,.T.);
#6536=ORIENTED_EDGE('',*,*,#4904,.T.);
#6537=ORIENTED_EDGE('',*,*,#4906,.F.);
#6538=ORIENTED_EDGE('',*,*,#4907,.F.);
#6539=ORIENTED_EDGE('',*,*,#4908,.T.);
#6540=ORIENTED_EDGE('',*,*,#4909,.T.);
#6541=ORIENTED_EDGE('',*,*,#4908,.F.);
#6542=ORIENTED_EDGE('',*,*,#4907,.T.);
#6543=ORIENTED_EDGE('',*,*,#4905,.T.);
#6544=ORIENTED_EDGE('',*,*,#4909,.F.);
#6545=ORIENTED_EDGE('',*,*,#4903,.F.);
#7167=CYLINDRICAL_SURFACE('',#8415,1.5);
#7168=CYLINDRICAL_SURFACE('',#8420,1.2);
#7169=CYLINDRICAL_SURFACE('',#8422,2.);
#7475=ADVANCED_FACE('',(#1274),#7167,.T.);
#7476=ADVANCED_FACE('',(#1275,#661),#924,.F.);
#7477=ADVANCED_FACE('',(#1276),#7168,.F.);
#7478=ADVANCED_FACE('',(#1277),#7169,.T.);
#7479=ADVANCED_FACE('',(#1278,#662),#925,.T.);
#7480=ADVANCED_FACE('',(#1279,#663),#926,.F.);
#7647=CLOSED_SHELL('',(#7475,#7476,#7477,#7478,#7479,#7480));
#8414=AXIS2_PLACEMENT_3D('',#12634,#10124,#10125);
#8415=AXIS2_PLACEMENT_3D('',#12635,#10126,#10127);
#8416=AXIS2_PLACEMENT_3D('',#12637,#10128,#10129);
#8417=AXIS2_PLACEMENT_3D('',#12640,#10131,#10132);
#8418=AXIS2_PLACEMENT_3D('',#12641,#10133,#10134);
#8419=AXIS2_PLACEMENT_3D('',#12643,#10135,#10136);
#8420=AXIS2_PLACEMENT_3D('',#12644,#10137,#10138);
#8421=AXIS2_PLACEMENT_3D('',#12646,#10139,#10140);
#8422=AXIS2_PLACEMENT_3D('',#12648,#10142,#10143);
#8423=AXIS2_PLACEMENT_3D('',#12650,#10144,#10145);
#8424=AXIS2_PLACEMENT_3D('',#12653,#10147,#10148);
#8425=AXIS2_PLACEMENT_3D('',#12654,#10149,#10150);
#8426=AXIS2_PLACEMENT_3D('',#12655,#10151,#10152);
#10124=DIRECTION('axis',(0.,0.,1.));
#10125=DIRECTION('refdir',(1.,0.,0.));
#10126=DIRECTION('center_axis',(0.,1.,0.));
#10127=DIRECTION('ref_axis',(1.,0.,0.));
#10128=DIRECTION('center_axis',(0.,-1.,0.));
#10129=DIRECTION('ref_axis',(1.,0.,0.));
#10130=DIRECTION('',(0.,1.,0.));
#10131=DIRECTION('center_axis',(0.,-1.,0.));
#10132=DIRECTION('ref_axis',(1.,0.,0.));
#10133=DIRECTION('center_axis',(0.,1.,0.));
#10134=DIRECTION('ref_axis',(1.,0.,0.));
#10135=DIRECTION('center_axis',(0.,-1.,0.));
#10136=DIRECTION('ref_axis',(1.,0.,0.));
#10137=DIRECTION('center_axis',(0.,1.,0.));
#10138=DIRECTION('ref_axis',(1.,0.,0.));
#10139=DIRECTION('center_axis',(0.,-1.,0.));
#10140=DIRECTION('ref_axis',(1.,0.,0.));
#10141=DIRECTION('',(0.,-1.,0.));
#10142=DIRECTION('center_axis',(0.,1.,0.));
#10143=DIRECTION('ref_axis',(1.,0.,0.));
#10144=DIRECTION('center_axis',(0.,1.,0.));
#10145=DIRECTION('ref_axis',(1.,0.,0.));
#10146=DIRECTION('',(0.,-1.,0.));
#10147=DIRECTION('center_axis',(0.,1.,0.));
#10148=DIRECTION('ref_axis',(1.,0.,0.));
#10149=DIRECTION('center_axis',(0.,1.,0.));
#10150=DIRECTION('ref_axis',(1.,0.,0.));
#10151=DIRECTION('center_axis',(0.,1.,0.));
#10152=DIRECTION('ref_axis',(1.,0.,0.));
#12634=CARTESIAN_POINT('',(0.,0.,0.));
#12635=CARTESIAN_POINT('Origin',(3.,29.95,8.));
#12636=CARTESIAN_POINT('',(1.5,29.95,8.));
#12637=CARTESIAN_POINT('Origin',(3.,29.95,8.));
#12638=CARTESIAN_POINT('',(1.5,30.,8.));
#12639=CARTESIAN_POINT('',(1.5,29.95,8.));
#12640=CARTESIAN_POINT('Origin',(3.,30.,8.));
#12641=CARTESIAN_POINT('Origin',(3.,29.95,8.));
#12642=CARTESIAN_POINT('',(1.8,29.95,8.));
#12643=CARTESIAN_POINT('Origin',(3.,29.95,8.));
#12644=CARTESIAN_POINT('Origin',(3.,30.,8.));
#12645=CARTESIAN_POINT('',(1.8,30.2,8.));
#12646=CARTESIAN_POINT('Origin',(3.,30.2,8.));
#12647=CARTESIAN_POINT('',(1.8,30.,8.));
#12648=CARTESIAN_POINT('Origin',(3.,30.,8.));
#12649=CARTESIAN_POINT('',(1.,30.2,8.));
#12650=CARTESIAN_POINT('Origin',(3.,30.2,8.));
#12651=CARTESIAN_POINT('',(1.,30.,8.));
#12652=CARTESIAN_POINT('',(1.,30.,8.));
#12653=CARTESIAN_POINT('Origin',(3.,30.,8.));
#12654=CARTESIAN_POINT('Origin',(3.,30.2,8.));
#12655=CARTESIAN_POINT('Origin',(3.,30.,8.));
#13765=UNCERTAINTY_MEASURE_WITH_UNIT(LENGTH_MEASURE(0.001),#13822,
'DISTANCE_ACCURACY_VALUE',
'Maximum model space distance between geometric entities at asserted c
onnectivities');
#13782=UNCERTAINTY_MEASURE_WITH_UNIT(LENGTH_MEASURE(0.001),#13822,
'DISTANCE_ACCURACY_VALUE',
'Maximum model space distance between geometric entities at asserted c
onnectivities');
#13804=(
GEOMETRIC_REPRESENTATION_CONTEXT(3)
GLOBAL_UNCERTAINTY_ASSIGNED_CONTEXT((#13765))
GLOBAL_UNIT_ASSIGNED_CONTEXT((#13822,#13824,#13825))
REPRESENTATION_CONTEXT('','3D')
);
#13821=(
GEOMETRIC_REPRESENTATION_CONTEXT(3)
GLOBAL_UNCERTAINTY_ASSIGNED_CONTEXT((#13782))
GLOBAL_UNIT_ASSIGNED_CONTEXT((#13822,#13824,#13825))
REPRESENTATION_CONTEXT('','3D')
);
#13822=(
LENGTH_UNIT()
NAMED_UNIT(*)
SI_UNIT(.CENTI.,.METRE.)
);
#13824=(
NAMED_UNIT(*)
PLANE_ANGLE_UNIT()
SI_UNIT($,.RADIAN.)
);
#13825=(
NAMED_UNIT(*)
SI_UNIT($,.STERADIAN.)
SOLID_ANGLE_UNIT()
);
#13847=SHAPE_DEFINITION_REPRESENTATION(#13885,#14017);
#13885=PRODUCT_DEFINITION_SHAPE('',$,#14056);
#14017=SHAPE_REPRESENTATION('',(#8414),#13804);
#14034=PRODUCT_DEFINITION_CONTEXT('part definition',#14150,'design');
#14056=PRODUCT_DEFINITION('Bearing retainer_1','Bearing retainer (1)',#14094,
#14034);
#14094=PRODUCT_DEFINITION_FORMATION('',$,#14173);
#14150=APPLICATION_CONTEXT(
'Core Data for Automotive Mechanical Design Process');
#14151=PRODUCT_CONTEXT('part definition',#14150,'mechanical');
#14173=PRODUCT('Bearing retainer_1','Bearing retainer (1)',
'Bearing retainer',(#14151));
#14191=PRESENTATION_STYLE_ASSIGNMENT((#14196));
#14196=SURFACE_STYLE_USAGE(.BOTH.,#14201);
#14201=SURFACE_SIDE_STYLE('',(#14206));
#14206=SURFACE_STYLE_FILL_AREA(#14211);
#14211=FILL_AREA_STYLE('CAD Library Painted - Steel gray',(#14216));
#14216=FILL_AREA_STYLE_COLOUR('CAD Library Painted - Steel gray',#14221);
#14221=COLOUR_RGB('CAD Library Painted - Steel gray',0.592156862745098,
0.631372549019608,0.67843137254902);
ENDSEC;
END-ISO-10303-21;
